ISO-10303-21;
HEADER;
FILE_DESCRIPTION (('STEP AP214'),
    '1' );
FILE_NAME ('Base Mounting Flange Control Box Bracket small.step',
    '2026-10-28T18:30:06',
    ( '' ),
    ( '' ),
    'SwSTEP 2.0',
    'SolidWorks 2024',
    '' );
FILE_SCHEMA (( 'AUTOMOTIVE_DESIGN' ));
ENDSEC;

DATA;
#16=CARTESIAN_POINT ( 'NONE',  ( 29.23877717791895492, 0.000000000000000000, 67.09613410133256650 ) ) ;
#29=CIRCLE ( 'NONE', #5298, 39.24395386344908587 ) ;
#37=AXIS2_PLACEMENT_3D ( 'NONE', #784, #1656, #4559 ) ;
#53=CARTESIAN_POINT ( 'NONE',  ( -60.76122282208098824, 0.000000000000000000, 167.0961341013325523 ) ) ;
#68=ORIENTED_EDGE ( 'NONE', *, *, #1541, .F. ) ;
#105=CARTESIAN_POINT ( 'NONE',  ( 29.23877717791895492, -14.99999999999998579, 67.09613410133256650 ) ) ;
#148=CARTESIAN_POINT ( 'NONE',  ( 29.23877717791895492, -14.99999999999998579, 117.0961341013325665 ) ) ;
#152=ORIENTED_EDGE ( 'NONE', *, *, #1132, .F. ) ;
#154=CIRCLE ( 'NONE', #4288, 50.00000000000000000 ) ;
#159=EDGE_CURVE ( 'NONE', #2587, #907, #154, .T. ) ;
#172=EDGE_LOOP ( 'NONE', ( #3037, #3349, #934, #4546, #4818, #515 ) ) ;
#175=CARTESIAN_POINT ( 'NONE',  ( -38.26122282208103798, -14.99999999999998579, 131.6034880481681171 ) ) ;
#180=CARTESIAN_POINT ( 'NONE',  ( -77.50517668553013095, -14.99999999999998579, 131.6034880481681171 ) ) ;
#233=PLANE ( 'NONE',  #418 ) ;
#256=APPLICATION_CONTEXT ( 'automotive_design' ) ;
#267=DIRECTION ( 'NONE',  ( 0.000000000000000000, 0.000000000000000000, 1.000000000000000000 ) ) ;
#286=PLANE ( 'NONE',  #591 ) ;
#289=DIRECTION ( 'NONE',  ( 0.000000000000000000, 0.000000000000000000, 1.000000000000000000 ) ) ;
#292=AXIS2_PLACEMENT_3D ( 'NONE', #5415, #4190, #801 ) ;
#295=DIRECTION ( 'NONE',  ( 0.000000000000000000, 1.000000000000000000, 0.000000000000000000 ) ) ;
#300=ADVANCED_FACE ( 'NONE', ( #1281 ), #3439, .T. ) ;
#307=CIRCLE ( 'NONE', #1007, 67.50000000000001421 ) ;
#337=EDGE_LOOP ( 'NONE', ( #2365, #2394 ) ) ;
#352=LINE ( 'NONE', #5372, #902 ) ;
#357=EDGE_CURVE ( 'NONE', #895, #2803, #863, .T. ) ;
#386=CIRCLE ( 'NONE', #1522, 50.00000000000000000 ) ;
#392=ORIENTED_EDGE ( 'NONE', *, *, #3263, .T. ) ;
#414=EDGE_CURVE ( 'NONE', #1788, #4543, #3759, .T. ) ;
#418=AXIS2_PLACEMENT_3D ( 'NONE', #3239, #1138, #2812 ) ;
#442=CARTESIAN_POINT ( 'NONE',  ( 29.23877717791896202, -14.99999999999998579, 17.09613410133256650 ) ) ;
#443=CYLINDRICAL_SURFACE ( 'NONE', #292, 67.50000000000001421 ) ;
#479=DIRECTION ( 'NONE',  ( 0.000000000000000000, 0.000000000000000000, 1.000000000000000000 ) ) ;
#492=ORIENTED_EDGE ( 'NONE', *, *, #4304, .T. ) ;
#498=DIRECTION ( 'NONE',  ( 1.000000000000000000, 0.000000000000000000, 0.000000000000000000 ) ) ;
#515=ORIENTED_EDGE ( 'NONE', *, *, #725, .T. ) ;
#522=SHAPE_REPRESENTATION_RELATIONSHIP ( 'NONE' , 'NONE' ,  #4024, #2470 ) ;
#591=AXIS2_PLACEMENT_3D ( 'NONE', #1966, #2725, #5312 ) ;
#603=CARTESIAN_POINT ( 'NONE',  ( 29.23877717791896202, 0.000000000000000000, 17.09613410133256650 ) ) ;
#610=DIRECTION ( 'NONE',  ( 0.000000000000000000, 1.000000000000000000, 0.000000000000000000 ) ) ;
#628=AXIS2_PLACEMENT_3D ( 'NONE', #1117, #1975, #759 ) ;
#659=ORIENTED_EDGE ( 'NONE', *, *, #1753, .F. ) ;
#691=LINE ( 'NONE', #2788, #5061 ) ;
#697=VERTEX_POINT ( 'NONE', #2984 ) ;
#702=DIRECTION ( 'NONE',  ( 0.000000000000000000, 1.000000000000000000, 0.000000000000000000 ) ) ;
#724=( GEOMETRIC_REPRESENTATION_CONTEXT ( 3 ) GLOBAL_UNCERTAINTY_ASSIGNED_CONTEXT ( ( #1159 ) ) GLOBAL_UNIT_ASSIGNED_CONTEXT ( ( #1725, #3826, #3420 ) ) REPRESENTATION_CONTEXT ( 'NONE', 'WORKASPACE' ) );
#725=EDGE_CURVE ( 'NONE', #697, #3805, #3377, .T. ) ;
#734=ADVANCED_FACE ( 'NONE', ( #5038 ), #4148, .F. ) ;
#751=STYLED_ITEM('',(#5444),#1308);
#759=DIRECTION ( 'NONE',  ( 0.000000000000000000, 0.000000000000000000, 1.000000000000000000 ) ) ;
#784=CARTESIAN_POINT ( 'NONE',  ( 135.9827310413679413, -14.99999999999998579, 131.6034880481681171 ) ) ;
#785=FACE_OUTER_BOUND ( 'NONE', #4999, .T. ) ;
#794=EDGE_LOOP ( 'NONE', ( #68, #829, #4704, #5108 ) ) ;
#801=DIRECTION ( 'NONE',  ( 0.000000000000000000, 0.000000000000000000, 1.000000000000000000 ) ) ;
#815=APPLICATION_CONTEXT ( 'automotive_design' ) ;
#829=ORIENTED_EDGE ( 'NONE', *, *, #2234, .F. ) ;
#837=DIRECTION ( 'NONE',  ( 0.000000000000000000, -1.000000000000000000, 0.000000000000000000 ) ) ;
#853=ORIENTED_EDGE ( 'NONE', *, *, #4537, .F. ) ;
#863=CIRCLE ( 'NONE', #3943, 50.00000000000000000 ) ;
#885=CYLINDRICAL_SURFACE ( 'NONE', #4185, 50.00000000000000000 ) ;
#895=VERTEX_POINT ( 'NONE', #3517 ) ;
#902=VECTOR ( 'NONE', #295, 1000.000000000000000 ) ;
#907=VERTEX_POINT ( 'NONE', #148 ) ;
#934=ORIENTED_EDGE ( 'NONE', *, *, #3288, .T. ) ;
#947=ORIENTED_EDGE ( 'NONE', *, *, #2735, .F. ) ;
#959=DIRECTION ( 'NONE',  ( 0.000000000000000000, 0.000000000000000000, 1.000000000000000000 ) ) ;
#995=CYLINDRICAL_SURFACE ( 'NONE', #1865, 50.00000000000000000 ) ;
#1004=DIRECTION ( 'NONE',  ( 0.000000000000000000, 1.000000000000000000, 0.000000000000000000 ) ) ;
#1007=AXIS2_PLACEMENT_3D ( 'NONE', #4386, #610, #289 ) ;
#1021=CARTESIAN_POINT ( 'NONE',  ( -38.26122282208105219, 0.000000000000000000, 67.09613410133258071 ) ) ;
#1028=DIRECTION ( 'NONE',  ( 0.000000000000000000, 1.000000000000000000, 0.000000000000000000 ) ) ;
#1045=FACE_OUTER_BOUND ( 'NONE', #3554, .T. ) ;
#1046=EDGE_CURVE ( 'NONE', #3719, #1423, #691, .T. ) ;
#1058=FACE_OUTER_BOUND ( 'NONE', #794, .T. ) ;
#1061=AXIS2_PLACEMENT_3D ( 'NONE', #3273, #5260, #267 ) ;
#1101=ADVANCED_FACE ( 'NONE', ( #2844, #4838 ), #286, .T. ) ;
#1102=ADVANCED_FACE ( 'NONE', ( #1468, #1552 ), #233, .F. ) ;
#1115=CARTESIAN_POINT ( 'NONE',  ( 29.23877717791895492, -14.99999999999998579, 67.09613410133256650 ) ) ;
#1117=CARTESIAN_POINT ( 'NONE',  ( -77.50517668553013095, -14.99999999999998579, 131.6034880481681171 ) ) ;
#1132=EDGE_CURVE ( 'NONE', #2756, #3474, #4626, .T. ) ;
#1136=PRODUCT ( 'Base Mounting Flange Control Box Bracket small', 'Base Mounting Flange Control Box Bracket small', '', ( #1920 ) ) ;
#1138=DIRECTION ( 'NONE',  ( 0.000000000000000000, 1.000000000000000000, 0.000000000000000000 ) ) ;
#1159=UNCERTAINTY_MEASURE_WITH_UNIT (LENGTH_MEASURE( 1.000000000000000082E-05 ), #1725, 'distance_accuracy_value', 'NONE');
#1186=ORIENTED_EDGE ( 'NONE', *, *, #159, .F. ) ;
#1215=FACE_OUTER_BOUND ( 'NONE', #5269, .T. ) ;
#1220=DIRECTION ( 'NONE',  ( 0.000000000000000000, -1.000000000000000000, 0.000000000000000000 ) ) ;
#1264=EDGE_CURVE ( 'NONE', #1807, #697, #3307, .T. ) ;
#1281=FACE_OUTER_BOUND ( 'NONE', #2842, .T. ) ;
#1295=ADVANCED_FACE ( 'NONE', ( #4529 ), #885, .F. ) ;
#1302=ORIENTED_EDGE ( 'NONE', *, *, #1264, .F. ) ;
#1308=MANIFOLD_SOLID_BREP ( 'Boss-Extrude1', #4374 ) ;
#1311=DIRECTION ( 'NONE',  ( 0.000000000000000000, 0.000000000000000000, 1.000000000000000000 ) ) ;
#1319=ORIENTED_EDGE ( 'NONE', *, *, #1746, .T. ) ;
#1337=DIRECTION ( 'NONE',  ( 0.000000000000000000, 0.000000000000000000, -1.000000000000000000 ) ) ;
#1340=CIRCLE ( 'NONE', #2127, 39.24395386344908587 ) ;
#1347=DIRECTION ( 'NONE',  ( 1.000000000000000000, 0.000000000000000000, 0.000000000000000000 ) ) ;
#1353=VECTOR ( 'NONE', #2876, 1000.000000000000000 ) ;
#1366=LINE ( 'NONE', #175, #4060 ) ;
#1409=DIRECTION ( 'NONE',  ( 0.000000000000000000, 0.000000000000000000, 1.000000000000000000 ) ) ;
#1423=VERTEX_POINT ( 'NONE', #3285 ) ;
#1432=CARTESIAN_POINT ( 'NONE',  ( 29.23877717791896202, -14.99999999999998579, 17.09613410133256650 ) ) ;
#1444=CARTESIAN_POINT ( 'NONE',  ( -38.26122282208105219, -14.99999999999998579, 67.09613410133258071 ) ) ;
#1468=FACE_BOUND ( 'NONE', #337, .T. ) ;
#1496=ADVANCED_FACE ( 'NONE', ( #1215 ), #2428, .T. ) ;
#1501=SHAPE_DEFINITION_REPRESENTATION ( #2064, #4024 ) ;
#1522=AXIS2_PLACEMENT_3D ( 'NONE', #1614, #1638, #3330 ) ;
#1541=EDGE_CURVE ( 'NONE', #2151, #1807, #5073, .T. ) ;
#1552=FACE_OUTER_BOUND ( 'NONE', #3657, .T. ) ;
#1614=CARTESIAN_POINT ( 'NONE',  ( 29.23877717791895492, 0.000000000000000000, 67.09613410133256650 ) ) ;
#1630=CARTESIAN_POINT ( 'NONE',  ( 135.9827310413679413, -14.99999999999998579, 131.6034880481681171 ) ) ;
#1638=DIRECTION ( 'NONE',  ( 0.000000000000000000, 1.000000000000000000, 0.000000000000000000 ) ) ;
#1656=DIRECTION ( 'NONE',  ( 0.000000000000000000, 1.000000000000000000, 0.000000000000000000 ) ) ;
#1710=ORIENTED_EDGE ( 'NONE', *, *, #357, .T. ) ;
#1725=( LENGTH_UNIT ( ) NAMED_UNIT ( * ) SI_UNIT ( .MILLI., .METRE. ) );
#1735=DIRECTION ( 'NONE',  ( 0.000000000000000000, 1.000000000000000000, 0.000000000000000000 ) ) ;
#1742=CARTESIAN_POINT ( 'NONE',  ( 119.2387771779189478, 0.000000000000000000, 167.0961341013325523 ) ) ;
#1746=EDGE_CURVE ( 'NONE', #1423, #3805, #352, .T. ) ;
#1753=EDGE_CURVE ( 'NONE', #907, #2587, #3276, .T. ) ;
#1757=VECTOR ( 'NONE', #498, 1000.000000000000000 ) ;
#1772=ADVANCED_FACE ( 'NONE', ( #785 ), #3221, .F. ) ;
#1788=VERTEX_POINT ( 'NONE', #3247 ) ;
#1807=VERTEX_POINT ( 'NONE', #1742 ) ;
#1820=LINE ( 'NONE', #3008, #2584 ) ;
#1829=AXIS2_PLACEMENT_3D ( 'NONE', #2962, #2473, #1337 ) ;
#1830=DIRECTION ( 'NONE',  ( 0.000000000000000000, -1.000000000000000000, 0.000000000000000000 ) ) ;
#1832=DIRECTION ( 'NONE',  ( 1.000000000000000000, 0.000000000000000000, 0.000000000000000000 ) ) ;
#1850=LINE ( 'NONE', #1444, #4852 ) ;
#1851=DIRECTION ( 'NONE',  ( 0.000000000000000000, -1.000000000000000000, 0.000000000000000000 ) ) ;
#1865=AXIS2_PLACEMENT_3D ( 'NONE', #4756, #2781, #1409 ) ;
#1920=PRODUCT_CONTEXT ( 'NONE', #256, 'mechanical' ) ;
#1927=DIRECTION ( 'NONE',  ( 0.000000000000000000, 1.000000000000000000, 0.000000000000000000 ) ) ;
#1966=CARTESIAN_POINT ( 'NONE',  ( 29.23877717791895492, 0.000000000000000000, 67.09613410133256650 ) ) ;
#1967=DIRECTION ( 'NONE',  ( 0.000000000000000000, 1.000000000000000000, 0.000000000000000000 ) ) ;
#1975=DIRECTION ( 'NONE',  ( 0.000000000000000000, 1.000000000000000000, 0.000000000000000000 ) ) ;
#2017=ORIENTED_EDGE ( 'NONE', *, *, #414, .F. ) ;
#2022=CARTESIAN_POINT ( 'NONE',  ( 119.2387771779189478, -14.99999999999998579, 167.0961341013325523 ) ) ;
#2042=EDGE_CURVE ( 'NONE', #1788, #3474, #1366, .T. ) ;
#2051=DIRECTION ( 'NONE',  ( 0.000000000000000000, 0.000000000000000000, -1.000000000000000000 ) ) ;
#2064=PRODUCT_DEFINITION_SHAPE ( 'NONE', 'NONE',  #5408 ) ;
#2098=ORIENTED_EDGE ( 'NONE', *, *, #4790, .F. ) ;
#2127=AXIS2_PLACEMENT_3D ( 'NONE', #1630, #1220, #479 ) ;
#2136=AXIS2_PLACEMENT_3D ( 'NONE', #4511, #2868, #4188 ) ;
#2151=VERTEX_POINT ( 'NONE', #3595 ) ;
#2163=( GEOMETRIC_REPRESENTATION_CONTEXT ( 3 ) GLOBAL_UNCERTAINTY_ASSIGNED_CONTEXT ( ( #4463 ) ) GLOBAL_UNIT_ASSIGNED_CONTEXT ( ( #2821, #2353, #4472 ) ) REPRESENTATION_CONTEXT ( 'NONE', 'WORKASPACE' ) );
#2173=ORIENTED_EDGE ( 'NONE', *, *, #2386, .F. ) ;
#2234=EDGE_CURVE ( 'NONE', #4543, #2151, #3240, .T. ) ;
#2244=VERTEX_POINT ( 'NONE', #2022 ) ;
#2312=VECTOR ( 'NONE', #3965, 1000.000000000000000 ) ;
#2353=( NAMED_UNIT ( * ) PLANE_ANGLE_UNIT ( ) SI_UNIT ( $, .RADIAN. ) );
#2365=ORIENTED_EDGE ( 'NONE', *, *, #1753, .T. ) ;
#2386=EDGE_CURVE ( 'NONE', #2244, #3719, #1340, .T. ) ;
#2394=ORIENTED_EDGE ( 'NONE', *, *, #159, .T. ) ;
#2397=CARTESIAN_POINT ( 'NONE',  ( 119.2387771779189478, -14.99999999999998579, 167.0961341013325523 ) ) ;
#2428=PLANE ( 'NONE',  #2136 ) ;
#2429=CARTESIAN_POINT ( 'NONE',  ( 96.73877717791896202, -14.99999999999998579, 131.6034880481681171 ) ) ;
#2440=ORIENTED_EDGE ( 'NONE', *, *, #1746, .F. ) ;
#2464=CARTESIAN_POINT ( 'NONE',  ( -60.76122282208098824, -14.99999999999998579, 167.0961341013325523 ) ) ;
#2470=ADVANCED_BREP_SHAPE_REPRESENTATION ( '', ( #1308, #2926 ), #724 ) ;
#2473=DIRECTION ( 'NONE',  ( 1.000000000000000000, 0.000000000000000000, 0.000000000000000000 ) ) ;
#2492=EDGE_LOOP ( 'NONE', ( #853, #2440, #392, #492 ) ) ;
#2493=CARTESIAN_POINT ( 'NONE',  ( 96.73877717791896202, 0.000000000000000000, 67.09613410133256650 ) ) ;
#2584=VECTOR ( 'NONE', #3513, 1000.000000000000000 ) ;
#2587=VERTEX_POINT ( 'NONE', #442 ) ;
#2594=CARTESIAN_POINT ( 'NONE',  ( -38.26122282208103798, 0.000000000000000000, 131.6034880481681171 ) ) ;
#2700=LINE ( 'NONE', #4379, #2312 ) ;
#2710=ORIENTED_EDGE ( 'NONE', *, *, #3288, .F. ) ;
#2725=DIRECTION ( 'NONE',  ( 0.000000000000000000, 1.000000000000000000, 0.000000000000000000 ) ) ;
#2735=EDGE_CURVE ( 'NONE', #2587, #2803, #5166, .T. ) ;
#2748=ADVANCED_FACE ( 'NONE', ( #1045 ), #995, .F. ) ;
#2756=VERTEX_POINT ( 'NONE', #1021 ) ;
#2763=CARTESIAN_POINT ( 'NONE',  ( -77.50517668553013095, 0.000000000000000000, 131.6034880481681171 ) ) ;
#2781=DIRECTION ( 'NONE',  ( 0.000000000000000000, 1.000000000000000000, 0.000000000000000000 ) ) ;
#2788=CARTESIAN_POINT ( 'NONE',  ( 96.73877717791896202, -14.99999999999998579, 67.09613410133256650 ) ) ;
#2803=VERTEX_POINT ( 'NONE', #603 ) ;
#2812=DIRECTION ( 'NONE',  ( 0.000000000000000000, 0.000000000000000000, 1.000000000000000000 ) ) ;
#2821=( LENGTH_UNIT ( ) NAMED_UNIT ( * ) SI_UNIT ( .MILLI., .METRE. ) );
#2842=EDGE_LOOP ( 'NONE', ( #3584, #2900, #4842, #1319 ) ) ;
#2844=FACE_BOUND ( 'NONE', #3567, .T. ) ;
#2868=DIRECTION ( 'NONE',  ( -1.000000000000000000, 0.000000000000000000, 0.000000000000000000 ) ) ;
#2876=DIRECTION ( 'NONE',  ( 0.000000000000000000, 0.000000000000000000, 1.000000000000000000 ) ) ;
#2895=FACE_OUTER_BOUND ( 'NONE', #2492, .T. ) ;
#2900=ORIENTED_EDGE ( 'NONE', *, *, #4812, .F. ) ;
#2926=AXIS2_PLACEMENT_3D ( 'NONE', #4646, #959, #1347 ) ;
#2953=CARTESIAN_POINT ( 'NONE',  ( 29.23877717791895492, 0.000000000000000000, 67.09613410133256650 ) ) ;
#2954=ORIENTED_EDGE ( 'NONE', *, *, #1046, .F. ) ;
#2962=CARTESIAN_POINT ( 'NONE',  ( 96.73877717791896202, -14.99999999999998579, 67.09613410133256650 ) ) ;
#2984=CARTESIAN_POINT ( 'NONE',  ( 96.73877717791896202, 0.000000000000000000, 131.6034880481681171 ) ) ;
#3008=CARTESIAN_POINT ( 'NONE',  ( -60.76122282208098824, -14.99999999999998579, 167.0961341013325523 ) ) ;
#3036=VECTOR ( 'NONE', #2051, 1000.000000000000000 ) ;
#3037=ORIENTED_EDGE ( 'NONE', *, *, #4537, .T. ) ;
#3084=EDGE_CURVE ( 'NONE', #2803, #895, #386, .T. ) ;
#3087=ORIENTED_EDGE ( 'NONE', *, *, #4702, .F. ) ;
#3172=ORIENTED_EDGE ( 'NONE', *, *, #3084, .T. ) ;
#3221=CYLINDRICAL_SURFACE ( 'NONE', #628, 39.24395386344908587 ) ;
#3239=CARTESIAN_POINT ( 'NONE',  ( 29.23877717791895492, -14.99999999999998579, 67.09613410133256650 ) ) ;
#3240=LINE ( 'NONE', #4875, #3789 ) ;
#3247=CARTESIAN_POINT ( 'NONE',  ( -38.26122282208103798, -14.99999999999998579, 131.6034880481681171 ) ) ;
#3263=EDGE_CURVE ( 'NONE', #1423, #3802, #307, .T. ) ;
#3273=CARTESIAN_POINT ( 'NONE',  ( 29.23877717791895492, -14.99999999999998579, 67.09613410133256650 ) ) ;
#3276=CIRCLE ( 'NONE', #1061, 50.00000000000000000 ) ;
#3283=ORIENTED_EDGE ( 'NONE', *, *, #4790, .T. ) ;
#3285=CARTESIAN_POINT ( 'NONE',  ( 96.73877717791896202, -14.99999999999998579, 67.09613410133256650 ) ) ;
#3288=EDGE_CURVE ( 'NONE', #3474, #2151, #29, .T. ) ;
#3290=CIRCLE ( 'NONE', #5115, 67.50000000000001421 ) ;
#3307=CIRCLE ( 'NONE', #4518, 39.24395386344908587 ) ;
#3328=EDGE_CURVE ( 'NONE', #3802, #1788, #4119, .T. ) ;
#3330=DIRECTION ( 'NONE',  ( 0.000000000000000000, 0.000000000000000000, 1.000000000000000000 ) ) ;
#3349=ORIENTED_EDGE ( 'NONE', *, *, #1132, .T. ) ;
#3377=LINE ( 'NONE', #2493, #3036 ) ;
#3420=( NAMED_UNIT ( * ) SI_UNIT ( $, .STERADIAN. ) SOLID_ANGLE_UNIT ( ) );
#3439=PLANE ( 'NONE',  #1829 ) ;
#3474=VERTEX_POINT ( 'NONE', #2594 ) ;
#3495=DIRECTION ( 'NONE',  ( 0.000000000000000000, 0.000000000000000000, -1.000000000000000000 ) ) ;
#3505=VECTOR ( 'NONE', #5416, 1000.000000000000000 ) ;
#3508=ORIENTED_EDGE ( 'NONE', *, *, #3263, .F. ) ;
#3513=DIRECTION ( 'NONE',  ( 1.000000000000000000, 0.000000000000000000, 0.000000000000000000 ) ) ;
#3517=CARTESIAN_POINT ( 'NONE',  ( 29.23877717791895492, 0.000000000000000000, 117.0961341013325665 ) ) ;
#3540=DIRECTION ( 'NONE',  ( 0.000000000000000000, 0.000000000000000000, -1.000000000000000000 ) ) ;
#3554=EDGE_LOOP ( 'NONE', ( #947, #659, #3283, #1710 ) ) ;
#3567=EDGE_LOOP ( 'NONE', ( #4667, #4131 ) ) ;
#3569=DIRECTION ( 'NONE',  ( 0.000000000000000000, 0.000000000000000000, -1.000000000000000000 ) ) ;
#3584=ORIENTED_EDGE ( 'NONE', *, *, #725, .F. ) ;
#3595=CARTESIAN_POINT ( 'NONE',  ( -60.76122282208098824, 0.000000000000000000, 167.0961341013325523 ) ) ;
#3646=ORIENTED_EDGE ( 'NONE', *, *, #2042, .F. ) ;
#3657=EDGE_LOOP ( 'NONE', ( #3508, #2954, #2173, #3087, #2017, #5072 ) ) ;
#3681=DIRECTION ( 'NONE',  ( 0.000000000000000000, 0.000000000000000000, 1.000000000000000000 ) ) ;
#3719=VERTEX_POINT ( 'NONE', #5209 ) ;
#3724=ADVANCED_FACE ( 'NONE', ( #1058 ), #3978, .T. ) ;
#3752=CARTESIAN_POINT ( 'NONE',  ( 135.9827310413679413, 0.000000000000000000, 131.6034880481681171 ) ) ;
#3756=ORIENTED_EDGE ( 'NONE', *, *, #2386, .T. ) ;
#3759=CIRCLE ( 'NONE', #5414, 39.24395386344908587 ) ;
#3773=DIRECTION ( 'NONE',  ( 0.000000000000000000, 0.000000000000000000, 1.000000000000000000 ) ) ;
#3789=VECTOR ( 'NONE', #1967, 1000.000000000000000 ) ;
#3801=ORIENTED_EDGE ( 'NONE', *, *, #414, .T. ) ;
#3802=VERTEX_POINT ( 'NONE', #4415 ) ;
#3805=VERTEX_POINT ( 'NONE', #4905 ) ;
#3826=( NAMED_UNIT ( * ) PLANE_ANGLE_UNIT ( ) SI_UNIT ( $, .RADIAN. ) );
#3903=VECTOR ( 'NONE', #4022, 1000.000000000000000 ) ;
#3940=DIRECTION ( 'NONE',  ( 0.000000000000000000, 1.000000000000000000, 0.000000000000000000 ) ) ;
#3943=AXIS2_PLACEMENT_3D ( 'NONE', #16, #5069, #1311 ) ;
#3965=DIRECTION ( 'NONE',  ( 0.000000000000000000, 1.000000000000000000, 0.000000000000000000 ) ) ;
#3978=PLANE ( 'NONE',  #4608 ) ;
#4001=PRODUCT_DEFINITION_FORMATION_WITH_SPECIFIED_SOURCE ( 'ANY', '', #1136, .NOT_KNOWN. ) ;
#4022=DIRECTION ( 'NONE',  ( 0.000000000000000000, 1.000000000000000000, 0.000000000000000000 ) ) ;
#4024=SHAPE_REPRESENTATION ( 'Base Mounting Flange Control Box Bracket small', ( #2926 ), #724 ) ;
#4060=VECTOR ( 'NONE', #1004, 1000.000000000000000 ) ;
#4083=ORIENTED_EDGE ( 'NONE', *, *, #4812, .T. ) ;
#4119=LINE ( 'NONE', #5076, #1353 ) ;
#4121=ORIENTED_EDGE ( 'NONE', *, *, #2042, .T. ) ;
#4131=ORIENTED_EDGE ( 'NONE', *, *, #3084, .F. ) ;
#4148=CYLINDRICAL_SURFACE ( 'NONE', #37, 39.24395386344908587 ) ;
#4162=VECTOR ( 'NONE', #3940, 1000.000000000000000 ) ;
#4185=AXIS2_PLACEMENT_3D ( 'NONE', #1115, #4443, #3681 ) ;
#4188=DIRECTION ( 'NONE',  ( 0.000000000000000000, 0.000000000000000000, 1.000000000000000000 ) ) ;
#4190=DIRECTION ( 'NONE',  ( 0.000000000000000000, 1.000000000000000000, 0.000000000000000000 ) ) ;
#4215=CARTESIAN_POINT ( 'NONE',  ( -38.26122282208105219, 0.000000000000000000, 67.09613410133258071 ) ) ;
#4288=AXIS2_PLACEMENT_3D ( 'NONE', #105, #702, #5377 ) ;
#4304=EDGE_CURVE ( 'NONE', #3802, #2756, #1850, .T. ) ;
#4337=VECTOR ( 'NONE', #1927, 1000.000000000000000 ) ;
#4340=CARTESIAN_POINT ( 'NONE',  ( -60.76122282208098824, -14.99999999999998579, 167.0961341013325523 ) ) ;
#4374=CLOSED_SHELL ( 'NONE', ( #1295, #5350, #300, #734, #3724, #1772, #1496, #1102, #1101, #2748 ) ) ;
#4379=CARTESIAN_POINT ( 'NONE',  ( 29.23877717791895492, -14.99999999999998579, 117.0961341013325665 ) ) ;
#4386=CARTESIAN_POINT ( 'NONE',  ( 29.23877717791895492, -14.99999999999998579, 67.09613410133256650 ) ) ;
#4415=CARTESIAN_POINT ( 'NONE',  ( -38.26122282208105219, -14.99999999999998579, 67.09613410133258071 ) ) ;
#4434=LINE ( 'NONE', #2429, #4337 ) ;
#4443=DIRECTION ( 'NONE',  ( 0.000000000000000000, 1.000000000000000000, 0.000000000000000000 ) ) ;
#4463=UNCERTAINTY_MEASURE_WITH_UNIT (LENGTH_MEASURE( 1.000000000000000082E-05 ), #2821, 'distance_accuracy_value', 'NONE');
#4472=( NAMED_UNIT ( * ) SI_UNIT ( $, .STERADIAN. ) SOLID_ANGLE_UNIT ( ) );
#4511=CARTESIAN_POINT ( 'NONE',  ( -38.26122282208105219, -14.99999999999998579, 67.09613410133258071 ) ) ;
#4518=AXIS2_PLACEMENT_3D ( 'NONE', #3752, #837, #5054 ) ;
#4529=FACE_OUTER_BOUND ( 'NONE', #4917, .T. ) ;
#4537=EDGE_CURVE ( 'NONE', #3805, #2756, #3290, .T. ) ;
#4543=VERTEX_POINT ( 'NONE', #2464 ) ;
#4546=ORIENTED_EDGE ( 'NONE', *, *, #1541, .T. ) ;
#4559=DIRECTION ( 'NONE',  ( 0.000000000000000000, 0.000000000000000000, 1.000000000000000000 ) ) ;
#4608=AXIS2_PLACEMENT_3D ( 'NONE', #4340, #5156, #1832 ) ;
#4616=MECHANICAL_DESIGN_GEOMETRIC_PRESENTATION_REPRESENTATION('',(#751),#2163);
#4626=LINE ( 'NONE', #4215, #3505 ) ;
#4646=CARTESIAN_POINT ( 'NONE',  ( 0.000000000000000000, 0.000000000000000000, 0.000000000000000000 ) ) ;
#4667=ORIENTED_EDGE ( 'NONE', *, *, #357, .F. ) ;
#4685=ORIENTED_EDGE ( 'NONE', *, *, #2735, .T. ) ;
#4702=EDGE_CURVE ( 'NONE', #4543, #2244, #1820, .T. ) ;
#4704=ORIENTED_EDGE ( 'NONE', *, *, #4702, .T. ) ;
#4756=CARTESIAN_POINT ( 'NONE',  ( 29.23877717791895492, -14.99999999999998579, 67.09613410133256650 ) ) ;
#4790=EDGE_CURVE ( 'NONE', #907, #895, #2700, .T. ) ;
#4812=EDGE_CURVE ( 'NONE', #3719, #697, #4434, .T. ) ;
#4818=ORIENTED_EDGE ( 'NONE', *, *, #1264, .T. ) ;
#4838=FACE_OUTER_BOUND ( 'NONE', #172, .T. ) ;
#4842=ORIENTED_EDGE ( 'NONE', *, *, #1046, .T. ) ;
#4852=VECTOR ( 'NONE', #1028, 1000.000000000000000 ) ;
#4853=EDGE_CURVE ( 'NONE', #2244, #1807, #4916, .T. ) ;
#4875=CARTESIAN_POINT ( 'NONE',  ( -60.76122282208098824, -14.99999999999998579, 167.0961341013325523 ) ) ;
#4905=CARTESIAN_POINT ( 'NONE',  ( 96.73877717791896202, 0.000000000000000000, 67.09613410133256650 ) ) ;
#4916=LINE ( 'NONE', #2397, #3903 ) ;
#4917=EDGE_LOOP ( 'NONE', ( #1186, #4685, #3172, #2098 ) ) ;
#4999=EDGE_LOOP ( 'NONE', ( #2710, #3646, #3801, #5220 ) ) ;
#5038=FACE_OUTER_BOUND ( 'NONE', #5310, .T. ) ;
#5054=DIRECTION ( 'NONE',  ( 0.000000000000000000, 0.000000000000000000, 1.000000000000000000 ) ) ;
#5061=VECTOR ( 'NONE', #3569, 1000.000000000000000 ) ;
#5069=DIRECTION ( 'NONE',  ( 0.000000000000000000, 1.000000000000000000, 0.000000000000000000 ) ) ;
#5071=ORIENTED_EDGE ( 'NONE', *, *, #4304, .F. ) ;
#5072=ORIENTED_EDGE ( 'NONE', *, *, #3328, .F. ) ;
#5073=LINE ( 'NONE', #53, #1757 ) ;
#5076=CARTESIAN_POINT ( 'NONE',  ( -38.26122282208105219, -14.99999999999998579, 67.09613410133258071 ) ) ;
#5087=ORIENTED_EDGE ( 'NONE', *, *, #4853, .F. ) ;
#5108=ORIENTED_EDGE ( 'NONE', *, *, #4853, .T. ) ;
#5115=AXIS2_PLACEMENT_3D ( 'NONE', #2953, #1735, #3773 ) ;
#5156=DIRECTION ( 'NONE',  ( 0.000000000000000000, 0.000000000000000000, 1.000000000000000000 ) ) ;
#5166=LINE ( 'NONE', #1432, #4162 ) ;
#5209=CARTESIAN_POINT ( 'NONE',  ( 96.73877717791896202, -14.99999999999998579, 131.6034880481681171 ) ) ;
#5220=ORIENTED_EDGE ( 'NONE', *, *, #2234, .T. ) ;
#5224=PRODUCT_DEFINITION_CONTEXT ( 'detailed design', #815, 'design' ) ;
#5232=ORIENTED_EDGE ( 'NONE', *, *, #3328, .T. ) ;
#5260=DIRECTION ( 'NONE',  ( 0.000000000000000000, 1.000000000000000000, 0.000000000000000000 ) ) ;
#5269=EDGE_LOOP ( 'NONE', ( #152, #5071, #5232, #4121 ) ) ;
#5298=AXIS2_PLACEMENT_3D ( 'NONE', #2763, #1851, #3540 ) ;
#5310=EDGE_LOOP ( 'NONE', ( #1302, #5087, #3756, #4083 ) ) ;
#5312=DIRECTION ( 'NONE',  ( 0.000000000000000000, 0.000000000000000000, 1.000000000000000000 ) ) ;
#5350=ADVANCED_FACE ( 'NONE', ( #2895 ), #443, .T. ) ;
#5372=CARTESIAN_POINT ( 'NONE',  ( 96.73877717791896202, -14.99999999999998579, 67.09613410133256650 ) ) ;
#5377=DIRECTION ( 'NONE',  ( 0.000000000000000000, 0.000000000000000000, 1.000000000000000000 ) ) ;
#5408=PRODUCT_DEFINITION ( 'UNKNOWN', '', #4001, #5224 ) ;
#5414=AXIS2_PLACEMENT_3D ( 'NONE', #180, #1830, #3495 ) ;
#5415=CARTESIAN_POINT ( 'NONE',  ( 29.23877717791895492, -14.99999999999998579, 67.09613410133256650 ) ) ;
#5416=DIRECTION ( 'NONE',  ( 0.000000000000000000, 0.000000000000000000, 1.000000000000000000 ) ) ;
#5438=COLOUR_RGB('Dark Blue',0.08,0.2,0.34);
#5439=FILL_AREA_STYLE_COLOUR('',#5438);
#5440=FILL_AREA_STYLE('',(#5439));
#5441=SURFACE_STYLE_FILL_AREA(#5440);
#5442=SURFACE_SIDE_STYLE('',(#5441));
#5443=SURFACE_STYLE_USAGE(.BOTH.,#5442);
#5444=PRESENTATION_STYLE_ASSIGNMENT((#5443));
ENDSEC;
END-ISO-10303-21;
